ISO-10303-21;
HEADER;
/* Generated by software containing ST-Developer
 * from STEP Tools, Inc. (www.steptools.com) 
 */

FILE_DESCRIPTION(
/* description */ ('Ratchet and pawl hand winch drum'),
/* implementation_level */ '2;1');

FILE_NAME(
/* name */ 'Flat Washer - M8.step',
/* time_stamp */ '2026-10-27T12:42:58-07:00',
/* author */ (''),
/* organization */ (''),
/* preprocessor_version */ 'ST-DEVELOPER v20.2',
/* originating_system */ 'Autodesk Translation Framework v15.17.0.0',
/* authorisation */ '');

FILE_SCHEMA (('AUTOMOTIVE_DESIGN { 1 0 10303 214 3 1 1 }'));
ENDSEC;

DATA;
#10=MECHANICAL_DESIGN_GEOMETRIC_PRESENTATION_REPRESENTATION('',(#407),#11801);
#338=SHAPE_REPRESENTATION_RELATIONSHIP('SRR','None',#11965,#372);
#372=ADVANCED_BREP_SHAPE_REPRESENTATION('',(#442),#11782);
#407=STYLED_ITEM('',(#12220),#442);
#442=MANIFOLD_SOLID_BREP('Body1',#6284);
#560=FACE_BOUND('',#1470,.T.);
#561=FACE_BOUND('',#1472,.T.);
#702=PLANE('',#6999);
#703=PLANE('',#7000);
#1007=FACE_OUTER_BOUND('',#1467,.T.);
#1008=FACE_OUTER_BOUND('',#1468,.T.);
#1009=FACE_OUTER_BOUND('',#1469,.T.);
#1010=FACE_OUTER_BOUND('',#1471,.T.);
#1467=EDGE_LOOP('',(#4969,#4970,#4971,#4972));
#1468=EDGE_LOOP('',(#4973,#4974,#4975,#4976));
#1469=EDGE_LOOP('',(#4977));
#1470=EDGE_LOOP('',(#4978));
#1471=EDGE_LOOP('',(#4979));
#1472=EDGE_LOOP('',(#4980));
#1910=LINE('',#10438,#2421);
#1911=LINE('',#10444,#2422);
#2421=VECTOR('',#8203,0.42);
#2422=VECTOR('',#8210,0.8);
#2843=CIRCLE('',#6994,0.42);
#2844=CIRCLE('',#6995,0.42);
#2845=CIRCLE('',#6997,0.8);
#2846=CIRCLE('',#6998,0.8);
#3190=VERTEX_POINT('',#10435);
#3191=VERTEX_POINT('',#10437);
#3192=VERTEX_POINT('',#10441);
#3193=VERTEX_POINT('',#10443);
#3828=EDGE_CURVE('',#3190,#3190,#2843,.T.);
#3829=EDGE_CURVE('',#3190,#3191,#1910,.T.);
#3830=EDGE_CURVE('',#3191,#3191,#2844,.T.);
#3831=EDGE_CURVE('',#3192,#3192,#2845,.T.);
#3832=EDGE_CURVE('',#3192,#3193,#1911,.T.);
#3833=EDGE_CURVE('',#3193,#3193,#2846,.T.);
#4969=ORIENTED_EDGE('',*,*,#3828,.F.);
#4970=ORIENTED_EDGE('',*,*,#3829,.T.);
#4971=ORIENTED_EDGE('',*,*,#3830,.T.);
#4972=ORIENTED_EDGE('',*,*,#3829,.F.);
#4973=ORIENTED_EDGE('',*,*,#3831,.F.);
#4974=ORIENTED_EDGE('',*,*,#3832,.T.);
#4975=ORIENTED_EDGE('',*,*,#3833,.T.);
#4976=ORIENTED_EDGE('',*,*,#3832,.F.);
#4977=ORIENTED_EDGE('',*,*,#3831,.T.);
#4978=ORIENTED_EDGE('',*,*,#3828,.T.);
#4979=ORIENTED_EDGE('',*,*,#3833,.F.);
#4980=ORIENTED_EDGE('',*,*,#3830,.F.);
#5871=CYLINDRICAL_SURFACE('',#6993,0.42);
#5872=CYLINDRICAL_SURFACE('',#6996,0.8);
#6077=ADVANCED_FACE('',(#1007),#5871,.F.);
#6078=ADVANCED_FACE('',(#1008),#5872,.T.);
#6079=ADVANCED_FACE('',(#1009,#560),#702,.T.);
#6080=ADVANCED_FACE('',(#1010,#561),#703,.F.);
#6284=CLOSED_SHELL('',(#6077,#6078,#6079,#6080));
#6992=AXIS2_PLACEMENT_3D('',#10433,#8197,#8198);
#6993=AXIS2_PLACEMENT_3D('',#10434,#8199,#8200);
#6994=AXIS2_PLACEMENT_3D('',#10436,#8201,#8202);
#6995=AXIS2_PLACEMENT_3D('',#10439,#8204,#8205);
#6996=AXIS2_PLACEMENT_3D('',#10440,#8206,#8207);
#6997=AXIS2_PLACEMENT_3D('',#10442,#8208,#8209);
#6998=AXIS2_PLACEMENT_3D('',#10445,#8211,#8212);
#6999=AXIS2_PLACEMENT_3D('',#10446,#8213,#8214);
#7000=AXIS2_PLACEMENT_3D('',#10447,#8215,#8216);
#8197=DIRECTION('axis',(0.,0.,1.));
#8198=DIRECTION('refdir',(1.,0.,0.));
#8199=DIRECTION('center_axis',(0.,1.,0.));
#8200=DIRECTION('ref_axis',(1.,0.,0.));
#8201=DIRECTION('center_axis',(0.,-1.,0.));
#8202=DIRECTION('ref_axis',(1.,0.,0.));
#8203=DIRECTION('',(0.,-1.,0.));
#8204=DIRECTION('center_axis',(0.,-1.,0.));
#8205=DIRECTION('ref_axis',(1.,0.,0.));
#8206=DIRECTION('center_axis',(0.,1.,0.));
#8207=DIRECTION('ref_axis',(1.,0.,0.));
#8208=DIRECTION('center_axis',(0.,1.,0.));
#8209=DIRECTION('ref_axis',(1.,0.,0.));
#8210=DIRECTION('',(0.,-1.,0.));
#8211=DIRECTION('center_axis',(0.,1.,0.));
#8212=DIRECTION('ref_axis',(1.,0.,0.));
#8213=DIRECTION('center_axis',(0.,1.,0.));
#8214=DIRECTION('ref_axis',(1.,0.,0.));
#8215=DIRECTION('center_axis',(0.,1.,0.));
#8216=DIRECTION('ref_axis',(1.,0.,0.));
#10433=CARTESIAN_POINT('',(0.,0.,0.));
#10434=CARTESIAN_POINT('Origin',(0.,0.,0.));
#10435=CARTESIAN_POINT('',(-0.42,0.16,5.14351655641888E-17));
#10436=CARTESIAN_POINT('Origin',(0.,0.16,0.));
#10437=CARTESIAN_POINT('',(-0.42,0.,5.14351655641888E-17));
#10438=CARTESIAN_POINT('',(-0.42,0.,5.14351655641888E-17));
#10439=CARTESIAN_POINT('Origin',(0.,0.,0.));
#10440=CARTESIAN_POINT('Origin',(0.,0.,0.));
#10441=CARTESIAN_POINT('',(-0.8,0.16,9.79717439317883E-17));
#10442=CARTESIAN_POINT('Origin',(0.,0.16,0.));
#10443=CARTESIAN_POINT('',(-0.8,0.,9.79717439317883E-17));
#10444=CARTESIAN_POINT('',(-0.8,0.,9.79717439317883E-17));
#10445=CARTESIAN_POINT('Origin',(0.,0.,0.));
#10446=CARTESIAN_POINT('Origin',(0.,0.16,0.));
#10447=CARTESIAN_POINT('Origin',(0.,0.,0.));
#11742=UNCERTAINTY_MEASURE_WITH_UNIT(LENGTH_MEASURE(0.001),#11802,
'DISTANCE_ACCURACY_VALUE',
'Maximum model space distance between geometric entities at asserted c
onnectivities');
#11761=UNCERTAINTY_MEASURE_WITH_UNIT(LENGTH_MEASURE(0.001),#11802,
'DISTANCE_ACCURACY_VALUE',
'Maximum model space distance between geometric entities at asserted c
onnectivities');
#11782=(
GEOMETRIC_REPRESENTATION_CONTEXT(3)
GLOBAL_UNCERTAINTY_ASSIGNED_CONTEXT((#11742))
GLOBAL_UNIT_ASSIGNED_CONTEXT((#11802,#11804,#11805))
REPRESENTATION_CONTEXT('','3D')
);
#11801=(
GEOMETRIC_REPRESENTATION_CONTEXT(3)
GLOBAL_UNCERTAINTY_ASSIGNED_CONTEXT((#11761))
GLOBAL_UNIT_ASSIGNED_CONTEXT((#11802,#11804,#11805))
REPRESENTATION_CONTEXT('','3D')
);
#11802=(
LENGTH_UNIT()
NAMED_UNIT(*)
SI_UNIT(.CENTI.,.METRE.)
);
#11804=(
NAMED_UNIT(*)
PLANE_ANGLE_UNIT()
SI_UNIT($,.RADIAN.)
);
#11805=(
NAMED_UNIT(*)
SI_UNIT($,.STERADIAN.)
SOLID_ANGLE_UNIT()
);
#11826=SHAPE_DEFINITION_REPRESENTATION(#11867,#11965);
#11867=PRODUCT_DEFINITION_SHAPE('',$,#12005);
#11965=SHAPE_REPRESENTATION('',(#6992),#11782);
#11984=PRODUCT_DEFINITION_CONTEXT('part definition',#12103,'design');
#12005=PRODUCT_DEFINITION('Flat Washer - M8','Flat Washer - M8',#12044,
#11984);
#12044=PRODUCT_DEFINITION_FORMATION('',$,#12125);
#12103=APPLICATION_CONTEXT(
'Core Data for Automotive Mechanical Design Process');
#12104=PRODUCT_CONTEXT('part definition',#12103,'mechanical');
#12125=PRODUCT('Flat Washer - M8','Flat Washer - M8','Flat Washer - M8',
(#12104));
#12214=COLOUR_RGB('Black',0.12,0.14,0.17);
#12215=FILL_AREA_STYLE_COLOUR('',#12214);
#12216=FILL_AREA_STYLE('',(#12215));
#12217=SURFACE_STYLE_FILL_AREA(#12216);
#12218=SURFACE_SIDE_STYLE('',(#12217));
#12219=SURFACE_STYLE_USAGE(.BOTH.,#12218);
#12220=PRESENTATION_STYLE_ASSIGNMENT((#12219));
ENDSEC;
END-ISO-10303-21;
